ISO-10303-21;
HEADER;
/* Generated by software containing ST-Developer
 * from STEP Tools, Inc. (www.steptools.com) 
 */

FILE_DESCRIPTION(
/* description */ ('PAT-122'),
/* implementation_level */ '2;1');

FILE_NAME(
/* name */ 'Foot (2).step',
/* time_stamp */ '2026-10-29T20:20:12-07:00',
/* author */ (''),
/* organization */ (''),
/* preprocessor_version */ 'ST-DEVELOPER v20.2',
/* originating_system */ 'Autodesk Translation Framework v15.17.0.0',
/* authorisation */ '');

FILE_SCHEMA (('AUTOMOTIVE_DESIGN { 1 0 10303 214 3 1 1 }'));
ENDSEC;

DATA;
#10=MECHANICAL_DESIGN_GEOMETRIC_PRESENTATION_REPRESENTATION('',(#495),#10019);
#451=SHAPE_REPRESENTATION_RELATIONSHIP('SRR','None',#10172,#473);
#473=ADVANCED_BREP_SHAPE_REPRESENTATION('',(#517),#10001);
#495=STYLED_ITEM('',(#10362),#517);
#517=MANIFOLD_SOLID_BREP('Body1',#5617);
#539=FACE_BOUND('',#1144,.T.);
#540=FACE_BOUND('',#1146,.T.);
#617=PLANE('',#5926);
#618=PLANE('',#5927);
#841=FACE_OUTER_BOUND('',#1141,.T.);
#842=FACE_OUTER_BOUND('',#1142,.T.);
#843=FACE_OUTER_BOUND('',#1143,.T.);
#844=FACE_OUTER_BOUND('',#1145,.T.);
#1141=EDGE_LOOP('',(#3913,#3914,#3915,#3916));
#1142=EDGE_LOOP('',(#3917,#3918,#3919,#3920));
#1143=EDGE_LOOP('',(#3921));
#1144=EDGE_LOOP('',(#3922));
#1145=EDGE_LOOP('',(#3923));
#1146=EDGE_LOOP('',(#3924));
#1495=LINE('',#8124,#2039);
#1496=LINE('',#8130,#2040);
#2039=VECTOR('',#6514,0.274999999999999);
#2040=VECTOR('',#6521,2.);
#2591=CIRCLE('',#5921,0.274999999999999);
#2592=CIRCLE('',#5922,0.274999999999999);
#2593=CIRCLE('',#5924,2.);
#2594=CIRCLE('',#5925,2.);
#2721=VERTEX_POINT('',#8121);
#2722=VERTEX_POINT('',#8123);
#2723=VERTEX_POINT('',#8127);
#2724=VERTEX_POINT('',#8129);
#3191=EDGE_CURVE('',#2721,#2721,#2591,.T.);
#3192=EDGE_CURVE('',#2721,#2722,#1495,.T.);
#3193=EDGE_CURVE('',#2722,#2722,#2592,.T.);
#3194=EDGE_CURVE('',#2723,#2723,#2593,.T.);
#3195=EDGE_CURVE('',#2723,#2724,#1496,.T.);
#3196=EDGE_CURVE('',#2724,#2724,#2594,.T.);
#3913=ORIENTED_EDGE('',*,*,#3191,.F.);
#3914=ORIENTED_EDGE('',*,*,#3192,.T.);
#3915=ORIENTED_EDGE('',*,*,#3193,.T.);
#3916=ORIENTED_EDGE('',*,*,#3192,.F.);
#3917=ORIENTED_EDGE('',*,*,#3194,.F.);
#3918=ORIENTED_EDGE('',*,*,#3195,.T.);
#3919=ORIENTED_EDGE('',*,*,#3196,.T.);
#3920=ORIENTED_EDGE('',*,*,#3195,.F.);
#3921=ORIENTED_EDGE('',*,*,#3194,.T.);
#3922=ORIENTED_EDGE('',*,*,#3191,.T.);
#3923=ORIENTED_EDGE('',*,*,#3196,.F.);
#3924=ORIENTED_EDGE('',*,*,#3193,.F.);
#5269=CYLINDRICAL_SURFACE('',#5920,0.274999999999999);
#5270=CYLINDRICAL_SURFACE('',#5923,2.);
#5337=ADVANCED_FACE('',(#841),#5269,.F.);
#5338=ADVANCED_FACE('',(#842),#5270,.T.);
#5339=ADVANCED_FACE('',(#843,#539),#617,.T.);
#5340=ADVANCED_FACE('',(#844,#540),#618,.F.);
#5617=CLOSED_SHELL('',(#5337,#5338,#5339,#5340));
#5919=AXIS2_PLACEMENT_3D('',#8119,#6508,#6509);
#5920=AXIS2_PLACEMENT_3D('',#8120,#6510,#6511);
#5921=AXIS2_PLACEMENT_3D('',#8122,#6512,#6513);
#5922=AXIS2_PLACEMENT_3D('',#8125,#6515,#6516);
#5923=AXIS2_PLACEMENT_3D('',#8126,#6517,#6518);
#5924=AXIS2_PLACEMENT_3D('',#8128,#6519,#6520);
#5925=AXIS2_PLACEMENT_3D('',#8131,#6522,#6523);
#5926=AXIS2_PLACEMENT_3D('',#8132,#6524,#6525);
#5927=AXIS2_PLACEMENT_3D('',#8133,#6526,#6527);
#6508=DIRECTION('axis',(0.,0.,1.));
#6509=DIRECTION('refdir',(1.,0.,0.));
#6510=DIRECTION('center_axis',(0.,0.,1.));
#6511=DIRECTION('ref_axis',(1.,0.,0.));
#6512=DIRECTION('center_axis',(0.,0.,-1.));
#6513=DIRECTION('ref_axis',(1.,0.,0.));
#6514=DIRECTION('',(0.,0.,-1.));
#6515=DIRECTION('center_axis',(0.,0.,-1.));
#6516=DIRECTION('ref_axis',(1.,0.,0.));
#6517=DIRECTION('center_axis',(0.,0.,1.));
#6518=DIRECTION('ref_axis',(1.,0.,0.));
#6519=DIRECTION('center_axis',(0.,0.,1.));
#6520=DIRECTION('ref_axis',(1.,0.,0.));
#6521=DIRECTION('',(0.,0.,-1.));
#6522=DIRECTION('center_axis',(0.,0.,1.));
#6523=DIRECTION('ref_axis',(1.,0.,0.));
#6524=DIRECTION('center_axis',(0.,0.,1.));
#6525=DIRECTION('ref_axis',(1.,0.,0.));
#6526=DIRECTION('center_axis',(0.,0.,1.));
#6527=DIRECTION('ref_axis',(1.,0.,0.));
#8119=CARTESIAN_POINT('',(0.,0.,0.));
#8120=CARTESIAN_POINT('Origin',(19.,-19.,-0.8));
#8121=CARTESIAN_POINT('',(18.725,-19.,0.));
#8122=CARTESIAN_POINT('Origin',(19.,-19.,0.));
#8123=CARTESIAN_POINT('',(18.725,-19.,-0.8));
#8124=CARTESIAN_POINT('',(18.725,-19.,-0.8));
#8125=CARTESIAN_POINT('Origin',(19.,-19.,-0.8));
#8126=CARTESIAN_POINT('Origin',(19.,-19.,-0.8));
#8127=CARTESIAN_POINT('',(17.,-19.,0.));
#8128=CARTESIAN_POINT('Origin',(19.,-19.,0.));
#8129=CARTESIAN_POINT('',(17.,-19.,-0.8));
#8130=CARTESIAN_POINT('',(17.,-19.,-0.8));
#8131=CARTESIAN_POINT('Origin',(19.,-19.,-0.8));
#8132=CARTESIAN_POINT('Origin',(19.,-19.,0.));
#8133=CARTESIAN_POINT('Origin',(19.,-19.,-0.8));
#9977=UNCERTAINTY_MEASURE_WITH_UNIT(LENGTH_MEASURE(0.001),#10020,
'DISTANCE_ACCURACY_VALUE',
'Maximum model space distance between geometric entities at asserted c
onnectivities');
#9995=UNCERTAINTY_MEASURE_WITH_UNIT(LENGTH_MEASURE(0.001),#10020,
'DISTANCE_ACCURACY_VALUE',
'Maximum model space distance between geometric entities at asserted c
onnectivities');
#10001=(
GEOMETRIC_REPRESENTATION_CONTEXT(3)
GLOBAL_UNCERTAINTY_ASSIGNED_CONTEXT((#9977))
GLOBAL_UNIT_ASSIGNED_CONTEXT((#10020,#10022,#10023))
REPRESENTATION_CONTEXT('','3D')
);
#10019=(
GEOMETRIC_REPRESENTATION_CONTEXT(3)
GLOBAL_UNCERTAINTY_ASSIGNED_CONTEXT((#9995))
GLOBAL_UNIT_ASSIGNED_CONTEXT((#10020,#10022,#10023))
REPRESENTATION_CONTEXT('','3D')
);
#10020=(
LENGTH_UNIT()
NAMED_UNIT(*)
SI_UNIT(.CENTI.,.METRE.)
);
#10022=(
NAMED_UNIT(*)
PLANE_ANGLE_UNIT()
SI_UNIT($,.RADIAN.)
);
#10023=(
NAMED_UNIT(*)
SI_UNIT($,.STERADIAN.)
SOLID_ANGLE_UNIT()
);
#10029=SHAPE_DEFINITION_REPRESENTATION(#10052,#10172);
#10052=PRODUCT_DEFINITION_SHAPE('',$,#10196);
#10172=SHAPE_REPRESENTATION('',(#5919),#10001);
#10190=PRODUCT_DEFINITION_CONTEXT('part definition',#10261,'design');
#10196=PRODUCT_DEFINITION('Foot (2)','Foot (2)',#10219,
#10190);
#10219=PRODUCT_DEFINITION_FORMATION('',$,#10268);
#10261=APPLICATION_CONTEXT(
'Core Data for Automotive Mechanical Design Process');
#10262=PRODUCT_CONTEXT('part definition',#10261,'mechanical');
#10268=PRODUCT('Foot (2)','Foot (2)','Foot (2)',(#10262));
#10356=COLOUR_RGB('Off White',0.89,0.88,0.83);
#10357=FILL_AREA_STYLE_COLOUR('',#10356);
#10358=FILL_AREA_STYLE('',(#10357));
#10359=SURFACE_STYLE_FILL_AREA(#10358);
#10360=SURFACE_SIDE_STYLE('',(#10359));
#10361=SURFACE_STYLE_USAGE(.BOTH.,#10360);
#10362=PRESENTATION_STYLE_ASSIGNMENT((#10361));
ENDSEC;
END-ISO-10303-21;
